ISO-10303-21;
HEADER;
/* Generated by software containing ST-Developer
 * from STEP Tools, Inc. (www.steptools.com) 
 */

FILE_DESCRIPTION(
/* description */ ('PAT-096'),
/* implementation_level */ '2;1');

FILE_NAME(
/* name */ 'Socket Set Screw - M4x6.step',
/* time_stamp */ '2026-10-29T17:03:14-07:00',
/* author */ (''),
/* organization */ (''),
/* preprocessor_version */ 'ST-DEVELOPER v20.2',
/* originating_system */ 'Autodesk Translation Framework v15.17.0.0',
/* authorisation */ '');

FILE_SCHEMA (('AUTOMOTIVE_DESIGN { 1 0 10303 214 3 1 1 }'));
ENDSEC;

DATA;
#10=MECHANICAL_DESIGN_GEOMETRIC_PRESENTATION_REPRESENTATION('',(#417),#10650);
#320=CONICAL_SURFACE('',#6265,0.185,0.785398163397449);
#321=CONICAL_SURFACE('',#6269,0.1625,0.785398163397449);
#347=SHAPE_REPRESENTATION_RELATIONSHIP('SRR','None',#10808,#378);
#378=ADVANCED_BREP_SHAPE_REPRESENTATION('',(#455),#10626);
#417=STYLED_ITEM('',(#11071),#455);
#455=MANIFOLD_SOLID_BREP('Body1',#5551);
#541=FACE_BOUND('',#1350,.T.);
#677=PLANE('',#6256);
#678=PLANE('',#6257);
#679=PLANE('',#6258);
#680=PLANE('',#6259);
#681=PLANE('',#6260);
#682=PLANE('',#6261);
#683=PLANE('',#6262);
#684=PLANE('',#6263);
#685=PLANE('',#6271);
#938=FACE_OUTER_BOUND('',#1342,.T.);
#939=FACE_OUTER_BOUND('',#1343,.T.);
#940=FACE_OUTER_BOUND('',#1344,.T.);
#941=FACE_OUTER_BOUND('',#1345,.T.);
#942=FACE_OUTER_BOUND('',#1346,.T.);
#943=FACE_OUTER_BOUND('',#1347,.T.);
#944=FACE_OUTER_BOUND('',#1348,.T.);
#945=FACE_OUTER_BOUND('',#1349,.T.);
#946=FACE_OUTER_BOUND('',#1351,.T.);
#947=FACE_OUTER_BOUND('',#1352,.T.);
#948=FACE_OUTER_BOUND('',#1353,.T.);
#949=FACE_OUTER_BOUND('',#1354,.T.);
#1342=EDGE_LOOP('',(#4341,#4342,#4343,#4344));
#1343=EDGE_LOOP('',(#4345,#4346,#4347,#4348));
#1344=EDGE_LOOP('',(#4349,#4350,#4351,#4352));
#1345=EDGE_LOOP('',(#4353,#4354,#4355,#4356));
#1346=EDGE_LOOP('',(#4357,#4358,#4359,#4360));
#1347=EDGE_LOOP('',(#4361,#4362,#4363,#4364));
#1348=EDGE_LOOP('',(#4365,#4366,#4367,#4368,#4369,#4370));
#1349=EDGE_LOOP('',(#4371));
#1350=EDGE_LOOP('',(#4372,#4373,#4374,#4375,#4376,#4377));
#1351=EDGE_LOOP('',(#4378,#4379,#4380,#4381));
#1352=EDGE_LOOP('',(#4382,#4383,#4384,#4385));
#1353=EDGE_LOOP('',(#4386,#4387,#4388,#4389));
#1354=EDGE_LOOP('',(#4390));
#1715=LINE('',#9639,#2044);
#1716=LINE('',#9641,#2045);
#1717=LINE('',#9643,#2046);
#1718=LINE('',#9644,#2047);
#1719=LINE('',#9647,#2048);
#1720=LINE('',#9649,#2049);
#1721=LINE('',#9650,#2050);
#1722=LINE('',#9653,#2051);
#1723=LINE('',#9655,#2052);
#1724=LINE('',#9656,#2053);
#1725=LINE('',#9659,#2054);
#1726=LINE('',#9661,#2055);
#1727=LINE('',#9662,#2056);
#1728=LINE('',#9665,#2057);
#1729=LINE('',#9667,#2058);
#1730=LINE('',#9668,#2059);
#1731=LINE('',#9670,#2060);
#1732=LINE('',#9671,#2061);
#1733=LINE('',#9679,#2062);
#1734=LINE('',#9683,#2063);
#1735=LINE('',#9687,#2064);
#2044=VECTOR('',#7469,1.);
#2045=VECTOR('',#7470,1.);
#2046=VECTOR('',#7471,1.);
#2047=VECTOR('',#7472,1.);
#2048=VECTOR('',#7475,1.);
#2049=VECTOR('',#7476,1.);
#2050=VECTOR('',#7477,1.);
#2051=VECTOR('',#7480,1.);
#2052=VECTOR('',#7481,1.);
#2053=VECTOR('',#7482,1.);
#2054=VECTOR('',#7485,1.);
#2055=VECTOR('',#7486,1.);
#2056=VECTOR('',#7487,1.);
#2057=VECTOR('',#7490,1.);
#2058=VECTOR('',#7491,1.);
#2059=VECTOR('',#7492,1.);
#2060=VECTOR('',#7495,1.);
#2061=VECTOR('',#7496,1.);
#2062=VECTOR('',#7507,0.185);
#2063=VECTOR('',#7512,0.2);
#2064=VECTOR('',#7517,0.1625);
#2432=CIRCLE('',#6264,0.17);
#2433=CIRCLE('',#6266,0.1954);
#2434=CIRCLE('',#6268,0.1954);
#2435=CIRCLE('',#6270,0.125);
#2795=VERTEX_POINT('',#9637);
#2796=VERTEX_POINT('',#9638);
#2797=VERTEX_POINT('',#9640);
#2798=VERTEX_POINT('',#9642);
#2799=VERTEX_POINT('',#9646);
#2800=VERTEX_POINT('',#9648);
#2801=VERTEX_POINT('',#9652);
#2802=VERTEX_POINT('',#9654);
#2803=VERTEX_POINT('',#9658);
#2804=VERTEX_POINT('',#9660);
#2805=VERTEX_POINT('',#9664);
#2806=VERTEX_POINT('',#9666);
#2807=VERTEX_POINT('',#9674);
#2808=VERTEX_POINT('',#9677);
#2809=VERTEX_POINT('',#9681);
#2810=VERTEX_POINT('',#9685);
#3349=EDGE_CURVE('',#2795,#2796,#1715,.T.);
#3350=EDGE_CURVE('',#2795,#2797,#1716,.T.);
#3351=EDGE_CURVE('',#2797,#2798,#1717,.T.);
#3352=EDGE_CURVE('',#2796,#2798,#1718,.T.);
#3353=EDGE_CURVE('',#2799,#2795,#1719,.T.);
#3354=EDGE_CURVE('',#2799,#2800,#1720,.T.);
#3355=EDGE_CURVE('',#2800,#2797,#1721,.T.);
#3356=EDGE_CURVE('',#2801,#2799,#1722,.T.);
#3357=EDGE_CURVE('',#2801,#2802,#1723,.T.);
#3358=EDGE_CURVE('',#2802,#2800,#1724,.T.);
#3359=EDGE_CURVE('',#2803,#2801,#1725,.T.);
#3360=EDGE_CURVE('',#2803,#2804,#1726,.T.);
#3361=EDGE_CURVE('',#2804,#2802,#1727,.T.);
#3362=EDGE_CURVE('',#2805,#2803,#1728,.T.);
#3363=EDGE_CURVE('',#2805,#2806,#1729,.T.);
#3364=EDGE_CURVE('',#2806,#2804,#1730,.T.);
#3365=EDGE_CURVE('',#2796,#2805,#1731,.T.);
#3366=EDGE_CURVE('',#2798,#2806,#1732,.T.);
#3367=EDGE_CURVE('',#2807,#2807,#2432,.T.);
#3368=EDGE_CURVE('',#2808,#2808,#2433,.T.);
#3369=EDGE_CURVE('',#2808,#2807,#1733,.T.);
#3370=EDGE_CURVE('',#2809,#2809,#2434,.F.);
#3371=EDGE_CURVE('',#2809,#2808,#1734,.T.);
#3372=EDGE_CURVE('',#2810,#2810,#2435,.T.);
#3373=EDGE_CURVE('',#2810,#2809,#1735,.T.);
#4341=ORIENTED_EDGE('',*,*,#3349,.F.);
#4342=ORIENTED_EDGE('',*,*,#3350,.T.);
#4343=ORIENTED_EDGE('',*,*,#3351,.T.);
#4344=ORIENTED_EDGE('',*,*,#3352,.F.);
#4345=ORIENTED_EDGE('',*,*,#3353,.F.);
#4346=ORIENTED_EDGE('',*,*,#3354,.T.);
#4347=ORIENTED_EDGE('',*,*,#3355,.T.);
#4348=ORIENTED_EDGE('',*,*,#3350,.F.);
#4349=ORIENTED_EDGE('',*,*,#3356,.F.);
#4350=ORIENTED_EDGE('',*,*,#3357,.T.);
#4351=ORIENTED_EDGE('',*,*,#3358,.T.);
#4352=ORIENTED_EDGE('',*,*,#3354,.F.);
#4353=ORIENTED_EDGE('',*,*,#3359,.F.);
#4354=ORIENTED_EDGE('',*,*,#3360,.T.);
#4355=ORIENTED_EDGE('',*,*,#3361,.T.);
#4356=ORIENTED_EDGE('',*,*,#3357,.F.);
#4357=ORIENTED_EDGE('',*,*,#3362,.F.);
#4358=ORIENTED_EDGE('',*,*,#3363,.T.);
#4359=ORIENTED_EDGE('',*,*,#3364,.T.);
#4360=ORIENTED_EDGE('',*,*,#3360,.F.);
#4361=ORIENTED_EDGE('',*,*,#3365,.F.);
#4362=ORIENTED_EDGE('',*,*,#3352,.T.);
#4363=ORIENTED_EDGE('',*,*,#3366,.T.);
#4364=ORIENTED_EDGE('',*,*,#3363,.F.);
#4365=ORIENTED_EDGE('',*,*,#3366,.F.);
#4366=ORIENTED_EDGE('',*,*,#3351,.F.);
#4367=ORIENTED_EDGE('',*,*,#3355,.F.);
#4368=ORIENTED_EDGE('',*,*,#3358,.F.);
#4369=ORIENTED_EDGE('',*,*,#3361,.F.);
#4370=ORIENTED_EDGE('',*,*,#3364,.F.);
#4371=ORIENTED_EDGE('',*,*,#3367,.F.);
#4372=ORIENTED_EDGE('',*,*,#3349,.T.);
#4373=ORIENTED_EDGE('',*,*,#3365,.T.);
#4374=ORIENTED_EDGE('',*,*,#3362,.T.);
#4375=ORIENTED_EDGE('',*,*,#3359,.T.);
#4376=ORIENTED_EDGE('',*,*,#3356,.T.);
#4377=ORIENTED_EDGE('',*,*,#3353,.T.);
#4378=ORIENTED_EDGE('',*,*,#3368,.F.);
#4379=ORIENTED_EDGE('',*,*,#3369,.T.);
#4380=ORIENTED_EDGE('',*,*,#3367,.T.);
#4381=ORIENTED_EDGE('',*,*,#3369,.F.);
#4382=ORIENTED_EDGE('',*,*,#3370,.F.);
#4383=ORIENTED_EDGE('',*,*,#3371,.T.);
#4384=ORIENTED_EDGE('',*,*,#3368,.T.);
#4385=ORIENTED_EDGE('',*,*,#3371,.F.);
#4386=ORIENTED_EDGE('',*,*,#3372,.F.);
#4387=ORIENTED_EDGE('',*,*,#3373,.T.);
#4388=ORIENTED_EDGE('',*,*,#3370,.T.);
#4389=ORIENTED_EDGE('',*,*,#3373,.F.);
#4390=ORIENTED_EDGE('',*,*,#3372,.T.);
#5130=CYLINDRICAL_SURFACE('',#6267,0.1954);
#5343=ADVANCED_FACE('',(#938),#677,.F.);
#5344=ADVANCED_FACE('',(#939),#678,.F.);
#5345=ADVANCED_FACE('',(#940),#679,.F.);
#5346=ADVANCED_FACE('',(#941),#680,.F.);
#5347=ADVANCED_FACE('',(#942),#681,.F.);
#5348=ADVANCED_FACE('',(#943),#682,.F.);
#5349=ADVANCED_FACE('',(#944),#683,.F.);
#5350=ADVANCED_FACE('',(#945,#541),#684,.T.);
#5351=ADVANCED_FACE('',(#946),#320,.T.);
#5352=ADVANCED_FACE('',(#947),#5130,.T.);
#5353=ADVANCED_FACE('',(#948),#321,.T.);
#5354=ADVANCED_FACE('',(#949),#685,.T.);
#5551=CLOSED_SHELL('',(#5343,#5344,#5345,#5346,#5347,#5348,#5349,#5350,
#5351,#5352,#5353,#5354));
#6255=AXIS2_PLACEMENT_3D('',#9635,#7465,#7466);
#6256=AXIS2_PLACEMENT_3D('',#9636,#7467,#7468);
#6257=AXIS2_PLACEMENT_3D('',#9645,#7473,#7474);
#6258=AXIS2_PLACEMENT_3D('',#9651,#7478,#7479);
#6259=AXIS2_PLACEMENT_3D('',#9657,#7483,#7484);
#6260=AXIS2_PLACEMENT_3D('',#9663,#7488,#7489);
#6261=AXIS2_PLACEMENT_3D('',#9669,#7493,#7494);
#6262=AXIS2_PLACEMENT_3D('',#9672,#7497,#7498);
#6263=AXIS2_PLACEMENT_3D('',#9673,#7499,#7500);
#6264=AXIS2_PLACEMENT_3D('',#9675,#7501,#7502);
#6265=AXIS2_PLACEMENT_3D('',#9676,#7503,#7504);
#6266=AXIS2_PLACEMENT_3D('',#9678,#7505,#7506);
#6267=AXIS2_PLACEMENT_3D('',#9680,#7508,#7509);
#6268=AXIS2_PLACEMENT_3D('',#9682,#7510,#7511);
#6269=AXIS2_PLACEMENT_3D('',#9684,#7513,#7514);
#6270=AXIS2_PLACEMENT_3D('',#9686,#7515,#7516);
#6271=AXIS2_PLACEMENT_3D('',#9688,#7518,#7519);
#7465=DIRECTION('axis',(0.,0.,1.));
#7466=DIRECTION('refdir',(1.,0.,0.));
#7467=DIRECTION('center_axis',(0.866025403784439,0.,-0.5));
#7468=DIRECTION('ref_axis',(0.5,0.,0.866025403784439));
#7469=DIRECTION('',(0.5,0.,0.866025403784439));
#7470=DIRECTION('',(0.,-1.,0.));
#7471=DIRECTION('',(0.5,0.,0.866025403784439));
#7472=DIRECTION('',(0.,-1.,0.));
#7473=DIRECTION('center_axis',(1.20185167898973E-16,0.,-1.));
#7474=DIRECTION('ref_axis',(1.,0.,1.20185167898973E-16));
#7475=DIRECTION('',(1.,0.,1.20185167898973E-16));
#7476=DIRECTION('',(0.,-1.,0.));
#7477=DIRECTION('',(1.,0.,1.20185167898973E-16));
#7478=DIRECTION('center_axis',(-0.866025403784439,0.,-0.5));
#7479=DIRECTION('ref_axis',(0.5,0.,-0.866025403784439));
#7480=DIRECTION('',(0.5,0.,-0.866025403784439));
#7481=DIRECTION('',(0.,-1.,0.));
#7482=DIRECTION('',(0.5,0.,-0.866025403784439));
#7483=DIRECTION('center_axis',(-0.866025403784439,0.,0.5));
#7484=DIRECTION('ref_axis',(-0.5,0.,-0.866025403784439));
#7485=DIRECTION('',(-0.5,0.,-0.866025403784439));
#7486=DIRECTION('',(0.,-1.,0.));
#7487=DIRECTION('',(-0.5,0.,-0.866025403784439));
#7488=DIRECTION('center_axis',(-2.40370335797945E-16,0.,1.));
#7489=DIRECTION('ref_axis',(-1.,0.,-2.40370335797945E-16));
#7490=DIRECTION('',(-1.,0.,-2.40370335797945E-16));
#7491=DIRECTION('',(0.,-1.,0.));
#7492=DIRECTION('',(-1.,0.,-2.40370335797945E-16));
#7493=DIRECTION('center_axis',(0.866025403784439,0.,0.5));
#7494=DIRECTION('ref_axis',(-0.5,0.,0.866025403784439));
#7495=DIRECTION('',(-0.5,0.,0.866025403784439));
#7496=DIRECTION('',(-0.5,0.,0.866025403784439));
#7497=DIRECTION('center_axis',(0.,-1.,0.));
#7498=DIRECTION('ref_axis',(0.,0.,-1.));
#7499=DIRECTION('center_axis',(0.,1.,0.));
#7500=DIRECTION('ref_axis',(0.,0.,1.));
#7501=DIRECTION('center_axis',(0.,-1.,0.));
#7502=DIRECTION('ref_axis',(1.,0.,0.));
#7503=DIRECTION('center_axis',(0.,-1.,0.));
#7504=DIRECTION('ref_axis',(1.,0.,0.));
#7505=DIRECTION('center_axis',(0.,-1.,0.));
#7506=DIRECTION('ref_axis',(1.,0.,0.));
#7507=DIRECTION('',(0.707106781186548,0.707106781186547,8.65956056235494E-17));
#7508=DIRECTION('center_axis',(0.,-1.,0.));
#7509=DIRECTION('ref_axis',(1.,0.,0.));
#7510=DIRECTION('center_axis',(0.,1.,0.));
#7511=DIRECTION('ref_axis',(1.,0.,0.));
#7512=DIRECTION('',(0.,1.,0.));
#7513=DIRECTION('center_axis',(0.,1.,0.));
#7514=DIRECTION('ref_axis',(1.,0.,0.));
#7515=DIRECTION('center_axis',(0.,-1.,0.));
#7516=DIRECTION('ref_axis',(1.,0.,0.));
#7517=DIRECTION('',(-0.707106781186548,0.707106781186547,-8.65956056235494E-17));
#7518=DIRECTION('center_axis',(0.,-1.,0.));
#7519=DIRECTION('ref_axis',(0.,0.,-1.));
#9635=CARTESIAN_POINT('',(0.,0.,0.));
#9636=CARTESIAN_POINT('Origin',(0.0577350269189626,0.,-0.1));
#9637=CARTESIAN_POINT('',(0.0577350269189626,0.,-0.1));
#9638=CARTESIAN_POINT('',(0.115470053837925,0.,0.));
#9639=CARTESIAN_POINT('',(0.0934187836487032,0.,-0.0381939203391614));
#9640=CARTESIAN_POINT('',(0.0577350269189626,-0.2,-0.1));
#9641=CARTESIAN_POINT('',(0.0577350269189626,0.,-0.1));
#9642=CARTESIAN_POINT('',(0.115470053837925,-0.2,0.));
#9643=CARTESIAN_POINT('',(0.115470053837925,-0.2,0.));
#9644=CARTESIAN_POINT('',(0.115470053837925,0.,0.));
#9645=CARTESIAN_POINT('Origin',(-0.0577350269189626,0.,-0.1));
#9646=CARTESIAN_POINT('',(-0.0577350269189626,0.,-0.1));
#9647=CARTESIAN_POINT('',(0.0561324865405187,0.,-0.1));
#9648=CARTESIAN_POINT('',(-0.0577350269189626,-0.2,-0.1));
#9649=CARTESIAN_POINT('',(-0.0577350269189626,0.,-0.1));
#9650=CARTESIAN_POINT('',(0.0577350269189626,-0.2,-0.1));
#9651=CARTESIAN_POINT('Origin',(-0.115470053837925,0.,-1.38777878078145E-17));
#9652=CARTESIAN_POINT('',(-0.115470053837925,0.,-1.41410031829988E-17));
#9653=CARTESIAN_POINT('',(-0.0797862971081845,0.,-0.0618060796608387));
#9654=CARTESIAN_POINT('',(-0.115470053837925,-0.2,-1.38777878078145E-17));
#9655=CARTESIAN_POINT('',(-0.115470053837925,0.,-1.41410031829988E-17));
#9656=CARTESIAN_POINT('',(-0.0577350269189626,-0.2,-0.1));
#9657=CARTESIAN_POINT('Origin',(-0.0577350269189626,0.,0.1));
#9658=CARTESIAN_POINT('',(-0.0577350269189626,0.,0.1));
#9659=CARTESIAN_POINT('',(-0.0509187836487033,0.,0.111806079660839));
#9660=CARTESIAN_POINT('',(-0.0577350269189626,-0.2,0.1));
#9661=CARTESIAN_POINT('',(-0.0577350269189626,0.,0.1));
#9662=CARTESIAN_POINT('',(-0.115470053837925,-0.2,-1.41410031829988E-17));
#9663=CARTESIAN_POINT('Origin',(0.0577350269189626,0.,0.1));
#9664=CARTESIAN_POINT('',(0.0577350269189626,0.,0.1));
#9665=CARTESIAN_POINT('',(0.113867513459481,0.,0.1));
#9666=CARTESIAN_POINT('',(0.0577350269189626,-0.2,0.1));
#9667=CARTESIAN_POINT('',(0.0577350269189626,0.,0.1));
#9668=CARTESIAN_POINT('',(-0.0577350269189626,-0.2,0.1));
#9669=CARTESIAN_POINT('Origin',(0.115470053837925,0.,0.));
#9670=CARTESIAN_POINT('',(0.122286297108185,0.,-0.0118060796608386));
#9671=CARTESIAN_POINT('',(0.0577350269189626,-0.2,0.1));
#9672=CARTESIAN_POINT('Origin',(0.,-0.2,0.));
#9673=CARTESIAN_POINT('Origin',(0.17,0.,0.));
#9674=CARTESIAN_POINT('',(-0.17,-8.67361737988404E-18,-2.0818995585505E-17));
#9675=CARTESIAN_POINT('Origin',(0.,0.,0.));
#9676=CARTESIAN_POINT('Origin',(0.,-0.015,0.));
#9677=CARTESIAN_POINT('',(-0.1954,-0.0254,-2.39295984553393E-17));
#9678=CARTESIAN_POINT('Origin',(0.,-0.0254,0.));
#9679=CARTESIAN_POINT('',(-0.185,-0.015,-2.2655965784226E-17));
#9680=CARTESIAN_POINT('Origin',(0.,-0.2775,0.));
#9681=CARTESIAN_POINT('',(-0.1954,-0.5296,2.39295984553393E-17));
#9682=CARTESIAN_POINT('Origin',(0.,-0.5296,0.));
#9683=CARTESIAN_POINT('',(-0.1954,-0.2775,-2.39295984553393E-17));
#9684=CARTESIAN_POINT('Origin',(0.,-0.5625,0.));
#9685=CARTESIAN_POINT('',(-0.125,-0.6,-1.53080849893419E-17));
#9686=CARTESIAN_POINT('Origin',(0.,-0.6,0.));
#9687=CARTESIAN_POINT('',(-0.1625,-0.5625,-1.99005104861445E-17));
#9688=CARTESIAN_POINT('Origin',(0.,-0.6,0.));
#10587=UNCERTAINTY_MEASURE_WITH_UNIT(LENGTH_MEASURE(0.001),#10651,
'DISTANCE_ACCURACY_VALUE',
'Maximum model space distance between geometric entities at asserted c
onnectivities');
#10611=UNCERTAINTY_MEASURE_WITH_UNIT(LENGTH_MEASURE(0.001),#10651,
'DISTANCE_ACCURACY_VALUE',
'Maximum model space distance between geometric entities at asserted c
onnectivities');
#10626=(
GEOMETRIC_REPRESENTATION_CONTEXT(3)
GLOBAL_UNCERTAINTY_ASSIGNED_CONTEXT((#10587))
GLOBAL_UNIT_ASSIGNED_CONTEXT((#10651,#10653,#10654))
REPRESENTATION_CONTEXT('','3D')
);
#10650=(
GEOMETRIC_REPRESENTATION_CONTEXT(3)
GLOBAL_UNCERTAINTY_ASSIGNED_CONTEXT((#10611))
GLOBAL_UNIT_ASSIGNED_CONTEXT((#10651,#10653,#10654))
REPRESENTATION_CONTEXT('','3D')
);
#10651=(
LENGTH_UNIT()
NAMED_UNIT(*)
SI_UNIT(.CENTI.,.METRE.)
);
#10653=(
NAMED_UNIT(*)
PLANE_ANGLE_UNIT()
SI_UNIT($,.RADIAN.)
);
#10654=(
NAMED_UNIT(*)
SI_UNIT($,.STERADIAN.)
SOLID_ANGLE_UNIT()
);
#10669=SHAPE_DEFINITION_REPRESENTATION(#10712,#10808);
#10712=PRODUCT_DEFINITION_SHAPE('',$,#10847);
#10808=SHAPE_REPRESENTATION('',(#6255),#10626);
#10832=PRODUCT_DEFINITION_CONTEXT('part definition',#10948,'design');
#10847=PRODUCT_DEFINITION('Socket Set Screw - M4x6',
'Socket Set Screw - M4x6',#10885,#10832);
#10885=PRODUCT_DEFINITION_FORMATION('',$,#10964);
#10948=APPLICATION_CONTEXT(
'Core Data for Automotive Mechanical Design Process');
#10949=PRODUCT_CONTEXT('part definition',#10948,'mechanical');
#10964=PRODUCT('Socket Set Screw - M4x6','Socket Set Screw - M4x6',
'Socket Set Screw - M4x6',(#10949));
#11065=COLOUR_RGB('Black',0.12,0.14,0.17);
#11066=FILL_AREA_STYLE_COLOUR('',#11065);
#11067=FILL_AREA_STYLE('',(#11066));
#11068=SURFACE_STYLE_FILL_AREA(#11067);
#11069=SURFACE_SIDE_STYLE('',(#11068));
#11070=SURFACE_STYLE_USAGE(.BOTH.,#11069);
#11071=PRESENTATION_STYLE_ASSIGNMENT((#11070));
ENDSEC;
END-ISO-10303-21;
